ISO-10303-21;
HEADER;
/* Generated by software containing ST-Developer
 * from STEP Tools, Inc. (www.steptools.com) 
 */

FILE_DESCRIPTION(
/* description */ ('Wheel Holder-Mirrored'),
/* implementation_level */ '2;1');

FILE_NAME(
/* name */ 'Bearings + Bolt.step',
/* time_stamp */ '2026-10-07T09:01:46-07:00',
/* author */ (''),
/* organization */ (''),
/* preprocessor_version */ 'ST-DEVELOPER v20.2',
/* originating_system */ 'Autodesk Translation Framework v15.15.0.0',
/* authorisation */ '');

FILE_SCHEMA (('AUTOMOTIVE_DESIGN { 1 0 10303 214 3 1 1 }'));
ENDSEC;

DATA;
#10=MECHANICAL_DESIGN_GEOMETRIC_PRESENTATION_REPRESENTATION('',(#199),#3832);
#187=SHAPE_REPRESENTATION_RELATIONSHIP('SRR','None',#3864,#193);
#193=ADVANCED_BREP_SHAPE_REPRESENTATION('',(#205),#3827);
#199=STYLED_ITEM('',(#3903),#205);
#205=MANIFOLD_SOLID_BREP('Body1',#1784);
#231=PLANE('',#1878);
#232=PLANE('',#1879);
#281=FACE_OUTER_BOUND('',#389,.T.);
#282=FACE_OUTER_BOUND('',#390,.T.);
#283=FACE_OUTER_BOUND('',#391,.T.);
#389=EDGE_LOOP('',(#1177,#1178,#1179,#1180));
#390=EDGE_LOOP('',(#1181));
#391=EDGE_LOOP('',(#1182));
#502=LINE('',#2560,#595);
#595=VECTOR('',#2094,0.00762);
#692=CIRCLE('',#1876,0.00762);
#693=CIRCLE('',#1877,0.00762);
#754=VERTEX_POINT('',#2557);
#755=VERTEX_POINT('',#2559);
#915=EDGE_CURVE('',#754,#754,#692,.T.);
#916=EDGE_CURVE('',#754,#755,#502,.T.);
#917=EDGE_CURVE('',#755,#755,#693,.T.);
#1177=ORIENTED_EDGE('',*,*,#915,.T.);
#1178=ORIENTED_EDGE('',*,*,#916,.T.);
#1179=ORIENTED_EDGE('',*,*,#917,.F.);
#1180=ORIENTED_EDGE('',*,*,#916,.F.);
#1181=ORIENTED_EDGE('',*,*,#917,.T.);
#1182=ORIENTED_EDGE('',*,*,#915,.F.);
#1657=CYLINDRICAL_SURFACE('',#1875,0.00762);
#1687=ADVANCED_FACE('',(#281),#1657,.T.);
#1688=ADVANCED_FACE('',(#282),#231,.T.);
#1689=ADVANCED_FACE('',(#283),#232,.F.);
#1784=CLOSED_SHELL('',(#1687,#1688,#1689));
#1874=AXIS2_PLACEMENT_3D('',#2555,#2088,#2089);
#1875=AXIS2_PLACEMENT_3D('',#2556,#2090,#2091);
#1876=AXIS2_PLACEMENT_3D('',#2558,#2092,#2093);
#1877=AXIS2_PLACEMENT_3D('',#2561,#2095,#2096);
#1878=AXIS2_PLACEMENT_3D('',#2562,#2097,#2098);
#1879=AXIS2_PLACEMENT_3D('',#2563,#2099,#2100);
#2088=DIRECTION('axis',(0.,0.,1.));
#2089=DIRECTION('refdir',(1.,0.,0.));
#2090=DIRECTION('center_axis',(-1.,0.,0.));
#2091=DIRECTION('ref_axis',(0.,0.,1.));
#2092=DIRECTION('center_axis',(1.,0.,0.));
#2093=DIRECTION('ref_axis',(0.,0.,-1.));
#2094=DIRECTION('',(1.,0.,0.));
#2095=DIRECTION('center_axis',(1.,0.,0.));
#2096=DIRECTION('ref_axis',(0.,0.,-1.));
#2097=DIRECTION('center_axis',(1.,0.,0.));
#2098=DIRECTION('ref_axis',(0.,1.,0.));
#2099=DIRECTION('center_axis',(1.,0.,0.));
#2100=DIRECTION('ref_axis',(0.,1.,0.));
#2555=CARTESIAN_POINT('',(0.,0.,0.));
#2556=CARTESIAN_POINT('Origin',(0.03556,4.66590430475142E-19,0.));
#2557=CARTESIAN_POINT('',(-0.03556,4.66590430475142E-19,-0.00762));
#2558=CARTESIAN_POINT('Origin',(-0.03556,4.66590430475142E-19,0.));
#2559=CARTESIAN_POINT('',(0.03556,4.66590430475142E-19,-0.00762));
#2560=CARTESIAN_POINT('',(0.03556,-4.66590430475141E-19,-0.00762));
#2561=CARTESIAN_POINT('Origin',(0.03556,4.66590430475142E-19,0.));
#2562=CARTESIAN_POINT('Origin',(0.03556,0.,0.));
#2563=CARTESIAN_POINT('Origin',(-0.03556,0.,0.));
#3819=UNCERTAINTY_MEASURE_WITH_UNIT(LENGTH_MEASURE(1.E-5),#3833,
'DISTANCE_ACCURACY_VALUE',
'Maximum model space distance between geometric entities at asserted c
onnectivities');
#3824=UNCERTAINTY_MEASURE_WITH_UNIT(LENGTH_MEASURE(1.E-5),#3833,
'DISTANCE_ACCURACY_VALUE',
'Maximum model space distance between geometric entities at asserted c
onnectivities');
#3827=(
GEOMETRIC_REPRESENTATION_CONTEXT(3)
GLOBAL_UNCERTAINTY_ASSIGNED_CONTEXT((#3819))
GLOBAL_UNIT_ASSIGNED_CONTEXT((#3833,#3834,#3835))
REPRESENTATION_CONTEXT('','3D')
);
#3832=(
GEOMETRIC_REPRESENTATION_CONTEXT(3)
GLOBAL_UNCERTAINTY_ASSIGNED_CONTEXT((#3824))
GLOBAL_UNIT_ASSIGNED_CONTEXT((#3833,#3834,#3835))
REPRESENTATION_CONTEXT('','3D')
);
#3833=(
LENGTH_UNIT()
NAMED_UNIT(*)
SI_UNIT($,.METRE.)
);
#3834=(
NAMED_UNIT(*)
PLANE_ANGLE_UNIT()
SI_UNIT($,.RADIAN.)
);
#3835=(
NAMED_UNIT(*)
SI_UNIT($,.STERADIAN.)
SOLID_ANGLE_UNIT()
);
#3838=SHAPE_DEFINITION_REPRESENTATION(#3845,#3864);
#3845=PRODUCT_DEFINITION_SHAPE('',$,#3872);
#3864=SHAPE_REPRESENTATION('',(#1874),#3827);
#3869=PRODUCT_DEFINITION_CONTEXT('part definition',#3892,'design');
#3872=PRODUCT_DEFINITION('2026-10-07-15-36-10-785','Bearings + Bolt',#3879,
#3869);
#3879=PRODUCT_DEFINITION_FORMATION('',$,#3896);
#3892=APPLICATION_CONTEXT(
'Core Data for Automotive Mechanical Design Process');
#3893=PRODUCT_CONTEXT('part definition',#3892,'mechanical');
#3896=PRODUCT('2026-10-07-15-36-10-785','Bearings + Bolt',
'Bearings + Bolt',(#3893));
#3903=PRESENTATION_STYLE_ASSIGNMENT((#3909));
#3909=SURFACE_STYLE_USAGE(.BOTH.,#3915);
#3915=SURFACE_SIDE_STYLE('',(#3921));
#3921=SURFACE_STYLE_FILL_AREA(#3927);
#3927=FILL_AREA_STYLE('Opaque(234,234,234)',(#3933));
#3933=FILL_AREA_STYLE_COLOUR('Opaque(234,234,234)',#3939);
#3939=COLOUR_RGB('Opaque(234,234,234)', 0.66274510, 0.83137255, 0.94901961);
ENDSEC;
END-ISO-10303-21;
